ISO-10303-21;
HEADER;
/* Generated by software containing ST-Developer
 * from STEP Tools, Inc. (www.steptools.com) 
 */

FILE_DESCRIPTION(
/* description */ ('STEP AP214'),
/* implementation_level */ '2;1');

FILE_NAME(
/* name */ 'Lock Nut.step',
/* time_stamp */ '2026-11-15T14:49:54-08:00',
/* author */ (''),
/* organization */ (''),
/* preprocessor_version */ 'ST-DEVELOPER v20.2',
/* originating_system */ 'Autodesk Translation Framework v15.17.0.0',
/* authorisation */ '');

FILE_SCHEMA (('AUTOMOTIVE_DESIGN { 1 0 10303 214 3 1 1 }'));
ENDSEC;

DATA;
#10=MECHANICAL_DESIGN_GEOMETRIC_PRESENTATION_REPRESENTATION('',(#1112),#66721);
#128=B_SPLINE_CURVE_WITH_KNOTS('',3,(#40857,#40858,#40859,#40860,#40861,
#40862,#40863,#40864,#40865,#40866,#40867,#40868,#40869,#40870,#40871,#40872,
#40873,#40874),.UNSPECIFIED.,.F.,.F.,(4,2,2,2,2,2,2,2,4),(-0.905722607976354,
-0.830246578316982,-0.754770548657611,-0.679292810320923,-0.603815071984236,
-0.528337333647548,-0.45285959531086,-0.377383565651489,-0.301907535992118),
 .UNSPECIFIED.);
#129=B_SPLINE_CURVE_WITH_KNOTS('',3,(#40878,#40879,#40880,#40881,#40882,
#40883,#40884,#40885,#40886,#40887,#40888,#40889,#40890,#40891,#40892,#40893,
#40894,#40895,#40896),.UNSPECIFIED.,.F.,.F.,(4,2,2,2,3,2,2,2,4),(-0.301907535992118,
-0.226431506332747,-0.150955476673376,-0.0754777383366878,0.,0.0754777383366878,
0.150955476673376,0.226431506332747,0.301907535992118),.UNSPECIFIED.);
#130=B_SPLINE_CURVE_WITH_KNOTS('',3,(#40901,#40902,#40903,#40904,#40905,
#40906,#40907,#40908,#40909,#40910,#40911,#40912,#40913,#40914,#40915,#40916,
#40917,#40918),.UNSPECIFIED.,.F.,.F.,(4,2,2,2,2,2,2,2,4),(1.26929433930301,
1.33221818753319,1.39514203576337,1.45914762146349,1.52315320716361,1.58715879286373,
1.65116437856384,1.71408822679403,1.77701207502421),.UNSPECIFIED.);
#131=B_SPLINE_CURVE_WITH_KNOTS('',3,(#40919,#40920,#40921,#40922,#40923,
#40924,#40925,#40926,#40927,#40928,#40929,#40930,#40931,#40932,#40933,#40934,
#40935,#40936,#40937),.UNSPECIFIED.,.F.,.F.,(4,2,2,2,3,2,2,2,4),(0.761576603581804,
0.824500451811986,0.887424300042168,0.951429885742286,1.0154354714424,1.07944105714252,
1.14344664284264,1.20637049107282,1.26929433930301),.UNSPECIFIED.);
#132=B_SPLINE_CURVE_WITH_KNOTS('',3,(#40950,#40951,#40952,#40953,#40954,
#40955,#40956,#40957,#40958,#40959,#40960,#40961,#40962,#40963,#40964,#40965,
#40966,#40967),.UNSPECIFIED.,.F.,.F.,(4,2,2,2,2,2,2,2,4),(0.303203013616562,
0.378994323042483,0.454785632468405,0.530595829850764,0.606406027233124,
0.682216224615484,0.758026421997844,0.833817731423765,0.909609040849686),
 .UNSPECIFIED.);
#133=B_SPLINE_CURVE_WITH_KNOTS('',3,(#40968,#40969,#40970,#40971,#40972,
#40973,#40974,#40975,#40976,#40977,#40978,#40979,#40980,#40981,#40982,#40983,
#40984,#40985,#40986),.UNSPECIFIED.,.F.,.F.,(4,2,2,2,3,2,2,2,4),(-0.303203013616562,
-0.227411704190641,-0.151620394764719,-0.0758101973823597,0.,0.0758101973823597,
0.151620394764719,0.227411704190641,0.303203013616562),.UNSPECIFIED.);
#546=CONICAL_SURFACE('',#27603,1.,1.02974425867665);
#547=CONICAL_SURFACE('',#27612,2.,0.785398163397443);
#548=CONICAL_SURFACE('',#27613,1.25,0.785398163397442);
#549=CONICAL_SURFACE('',#27618,6.9585,0.78539816339745);
#550=CONICAL_SURFACE('',#27622,7.5,0.785398163397448);
#1050=SHAPE_REPRESENTATION_RELATIONSHIP('SRR','None',#66911,#1081);
#1081=ADVANCED_BREP_SHAPE_REPRESENTATION('',(#1147),#66702);
#1112=STYLED_ITEM('',(#67095),#1147);
#1147=MANIFOLD_SOLID_BREP('Body1',#25678);
#1373=FACE_BOUND('',#4721,.T.);
#1374=FACE_BOUND('',#4723,.T.);
#1375=FACE_BOUND('',#4725,.T.);
#1376=FACE_BOUND('',#4729,.T.);
#1377=FACE_BOUND('',#4731,.T.);
#1378=FACE_BOUND('',#4733,.T.);
#1982=PLANE('',#27648);
#1983=PLANE('',#27649);
#1984=PLANE('',#27650);
#1985=PLANE('',#27651);
#1986=PLANE('',#27652);
#1987=PLANE('',#27653);
#1988=PLANE('',#27654);
#1989=PLANE('',#27655);
#1990=PLANE('',#27656);
#1991=PLANE('',#27657);
#1992=PLANE('',#27658);
#1993=PLANE('',#27659);
#1994=PLANE('',#27660);
#1995=PLANE('',#27661);
#1996=PLANE('',#27662);
#1997=PLANE('',#27663);
#1998=PLANE('',#27664);
#1999=PLANE('',#27665);
#2000=PLANE('',#27666);
#2001=PLANE('',#27667);
#3064=FACE_OUTER_BOUND('',#4711,.T.);
#3065=FACE_OUTER_BOUND('',#4712,.T.);
#3066=FACE_OUTER_BOUND('',#4713,.T.);
#3067=FACE_OUTER_BOUND('',#4714,.T.);
#3068=FACE_OUTER_BOUND('',#4715,.T.);
#3069=FACE_OUTER_BOUND('',#4716,.T.);
#3070=FACE_OUTER_BOUND('',#4717,.T.);
#3071=FACE_OUTER_BOUND('',#4718,.T.);
#3072=FACE_OUTER_BOUND('',#4719,.T.);
#3073=FACE_OUTER_BOUND('',#4720,.T.);
#3074=FACE_OUTER_BOUND('',#4722,.T.);
#3075=FACE_OUTER_BOUND('',#4724,.T.);
#3076=FACE_OUTER_BOUND('',#4726,.T.);
#3077=FACE_OUTER_BOUND('',#4727,.T.);
#3078=FACE_OUTER_BOUND('',#4728,.T.);
#3079=FACE_OUTER_BOUND('',#4730,.T.);
#3080=FACE_OUTER_BOUND('',#4732,.T.);
#3081=FACE_OUTER_BOUND('',#4734,.T.);
#3082=FACE_OUTER_BOUND('',#4735,.T.);
#3083=FACE_OUTER_BOUND('',#4736,.T.);
#3084=FACE_OUTER_BOUND('',#4737,.T.);
#3085=FACE_OUTER_BOUND('',#4738,.T.);
#3086=FACE_OUTER_BOUND('',#4739,.T.);
#3087=FACE_OUTER_BOUND('',#4740,.T.);
#3088=FACE_OUTER_BOUND('',#4741,.T.);
#3089=FACE_OUTER_BOUND('',#4742,.T.);
#3090=FACE_OUTER_BOUND('',#4743,.T.);
#3091=FACE_OUTER_BOUND('',#4744,.T.);
#3092=FACE_OUTER_BOUND('',#4745,.T.);
#3093=FACE_OUTER_BOUND('',#4746,.T.);
#3094=FACE_OUTER_BOUND('',#4747,.T.);
#3095=FACE_OUTER_BOUND('',#4748,.T.);
#3096=FACE_OUTER_BOUND('',#4749,.T.);
#3097=FACE_OUTER_BOUND('',#4750,.T.);
#4711=EDGE_LOOP('',(#20804,#20805,#20806,#20807,#20808,#20809,#20810,#20811));
#4712=EDGE_LOOP('',(#20812,#20813,#20814,#20815,#20816));
#4713=EDGE_LOOP('',(#20817,#20818,#20819,#20820,#20821));
#4714=EDGE_LOOP('',(#20822,#20823,#20824,#20825,#20826));
#4715=EDGE_LOOP('',(#20827,#20828,#20829,#20830,#20831,#20832));
#4716=EDGE_LOOP('',(#20833,#20834,#20835,#20836,#20837));
#4717=EDGE_LOOP('',(#20838,#20839,#20840,#20841));
#4718=EDGE_LOOP('',(#20842,#20843,#20844,#20845));
#4719=EDGE_LOOP('',(#20846,#20847,#20848,#20849));
#4720=EDGE_LOOP('',(#20850,#20851,#20852,#20853,#20854));
#4721=EDGE_LOOP('',(#20855,#20856));
#4722=EDGE_LOOP('',(#20857,#20858));
#4723=EDGE_LOOP('',(#20859,#20860,#20861,#20862,#20863,#20864));
#4724=EDGE_LOOP('',(#20865,#20866,#20867,#20868));
#4725=EDGE_LOOP('',(#20869,#20870));
#4726=EDGE_LOOP('',(#20871,#20872,#20873,#20874));
#4727=EDGE_LOOP('',(#20875,#20876,#20877,#20878));
#4728=EDGE_LOOP('',(#20879));
#4729=EDGE_LOOP('',(#20880));
#4730=EDGE_LOOP('',(#20881,#20882,#20883,#20884,#20885,#20886,#20887,#20888));
#4731=EDGE_LOOP('',(#20889));
#4732=EDGE_LOOP('',(#20890,#20891,#20892,#20893,#20894,#20895,#20896,#20897));
#4733=EDGE_LOOP('',(#20898));
#4734=EDGE_LOOP('',(#20899,#20900,#20901,#20902));
#4735=EDGE_LOOP('',(#20903,#20904,#20905,#20906));
#4736=EDGE_LOOP('',(#20907,#20908,#20909,#20910));
#4737=EDGE_LOOP('',(#20911,#20912,#20913,#20914));
#4738=EDGE_LOOP('',(#20915));
#4739=EDGE_LOOP('',(#20916,#20917,#20918,#20919,#20920));
#4740=EDGE_LOOP('',(#20921,#20922,#20923,#20924,#20925));
#4741=EDGE_LOOP('',(#20926,#20927,#20928,#20929,#20930));
#4742=EDGE_LOOP('',(#20931,#20932,#20933,#20934,#20935));
#4743=EDGE_LOOP('',(#20936,#20937,#20938,#20939,#20940));
#4744=EDGE_LOOP('',(#20941,#20942,#20943,#20944,#20945));
#4745=EDGE_LOOP('',(#20946,#20947,#20948));
#4746=EDGE_LOOP('',(#20949,#20950,#20951));
#4747=EDGE_LOOP('',(#20952,#20953,#20954));
#4748=EDGE_LOOP('',(#20955,#20956,#20957));
#4749=EDGE_LOOP('',(#20958,#20959,#20960));
#4750=EDGE_LOOP('',(#20961,#20962,#20963));
#6811=LINE('',#40842,#8800);
#6812=LINE('',#40876,#8801);
#6813=LINE('',#40899,#8802);
#6814=LINE('',#40943,#8803);
#6815=LINE('',#40948,#8804);
#6816=LINE('',#40992,#8805);
#6817=LINE('',#40999,#8806);
#6818=LINE('',#41006,#8807);
#6819=LINE('',#41009,#8808);
#6820=LINE('',#41014,#8809);
#6821=LINE('',#41017,#8810);
#6822=LINE('',#41036,#8811);
#6823=LINE('',#41039,#8812);
#6824=LINE('',#41045,#8813);
#6825=LINE('',#41048,#8814);
#6826=LINE('',#41054,#8815);
#6827=LINE('',#41057,#8816);
#6828=LINE('',#41060,#8817);
#6829=LINE('',#41061,#8818);
#6830=LINE('',#41062,#8819);
#6831=LINE('',#41063,#8820);
#6832=LINE('',#41065,#8821);
#6833=LINE('',#41066,#8822);
#6834=LINE('',#41067,#8823);
#6835=LINE('',#41068,#8824);
#6836=LINE('',#41076,#8825);
#6837=LINE('',#41077,#8826);
#6838=LINE('',#41079,#8827);
#6839=LINE('',#41080,#8828);
#6840=LINE('',#41082,#8829);
#6841=LINE('',#41084,#8830);
#6842=LINE('',#41085,#8831);
#6843=LINE('',#41087,#8832);
#6844=LINE('',#41089,#8833);
#6845=LINE('',#41090,#8834);
#6846=LINE('',#41092,#8835);
#6847=LINE('',#41094,#8836);
#6848=LINE('',#41095,#8837);
#6849=LINE('',#41097,#8838);
#6850=LINE('',#41099,#8839);
#6851=LINE('',#41100,#8840);
#6852=LINE('',#41102,#8841);
#6853=LINE('',#41103,#8842);
#8800=VECTOR('',#33210,1.);
#8801=VECTOR('',#33225,2.);
#8802=VECTOR('',#33230,2.);
#8803=VECTOR('',#33235,1.25);
#8804=VECTOR('',#33242,2.);
#8805=VECTOR('',#33247,6.9585);
#8806=VECTOR('',#33256,7.5);
#8807=VECTOR('',#33263,1000.);
#8808=VECTOR('',#33266,1000.);
#8809=VECTOR('',#33271,10.5);
#8810=VECTOR('',#33276,6.9585);
#8811=VECTOR('',#33295,1000.);
#8812=VECTOR('',#33298,1000.);
#8813=VECTOR('',#33303,1000.);
#8814=VECTOR('',#33306,1000.);
#8815=VECTOR('',#33311,1000.);
#8816=VECTOR('',#33314,1000.);
#8817=VECTOR('',#33319,1000.);
#8818=VECTOR('',#33320,1000.);
#8819=VECTOR('',#33321,1000.);
#8820=VECTOR('',#33322,1000.);
#8821=VECTOR('',#33325,1000.);
#8822=VECTOR('',#33326,1000.);
#8823=VECTOR('',#33327,1000.);
#8824=VECTOR('',#33328,1000.);
#8825=VECTOR('',#33341,1000.);
#8826=VECTOR('',#33342,1000.);
#8827=VECTOR('',#33343,1000.);
#8828=VECTOR('',#33344,1000.);
#8829=VECTOR('',#33347,1000.);
#8830=VECTOR('',#33348,1000.);
#8831=VECTOR('',#33349,1000.);
#8832=VECTOR('',#33352,1000.);
#8833=VECTOR('',#33353,1000.);
#8834=VECTOR('',#33354,1000.);
#8835=VECTOR('',#33357,1000.);
#8836=VECTOR('',#33358,1000.);
#8837=VECTOR('',#33359,1000.);
#8838=VECTOR('',#33362,1000.);
#8839=VECTOR('',#33363,1000.);
#8840=VECTOR('',#33364,1000.);
#8841=VECTOR('',#33367,1000.);
#8842=VECTOR('',#33368,1000.);
#10116=CIRCLE('',#27604,1.);
#10117=CIRCLE('',#27605,1.);
#10118=CIRCLE('',#27606,1.);
#10119=CIRCLE('',#27607,1.);
#10120=CIRCLE('',#27608,1.);
#10121=CIRCLE('',#27609,1.);
#10122=CIRCLE('',#27611,2.);
#10123=CIRCLE('',#27614,2.);
#10124=CIRCLE('',#27615,1.25);
#10125=CIRCLE('',#27616,2.);
#10126=CIRCLE('',#27619,6.9585);
#10127=CIRCLE('',#27620,7.5);
#10128=CIRCLE('',#27621,6.9585);
#10129=CIRCLE('',#27623,6.9585);
#10130=CIRCLE('',#27624,7.5);
#10131=CIRCLE('',#27626,12.5);
#10132=CIRCLE('',#27627,12.5);
#10133=CIRCLE('',#27629,10.5);
#10134=CIRCLE('',#27630,10.5);
#10135=CIRCLE('',#27633,12.5);
#10136=CIRCLE('',#27634,49.725094979045);
#10137=CIRCLE('',#27635,49.7250949790431);
#10138=CIRCLE('',#27636,12.5);
#10139=CIRCLE('',#27637,49.7250949790141);
#10140=CIRCLE('',#27638,49.7250949790647);
#10141=CIRCLE('',#27640,12.5);
#10142=CIRCLE('',#27641,12.5);
#10143=CIRCLE('',#27643,12.5);
#10144=CIRCLE('',#27644,12.5);
#10145=CIRCLE('',#27646,12.5);
#10146=CIRCLE('',#27647,12.5);
#12031=VERTEX_POINT('',#40840);
#12032=VERTEX_POINT('',#40841);
#12033=VERTEX_POINT('',#40843);
#12034=VERTEX_POINT('',#40845);
#12035=VERTEX_POINT('',#40847);
#12036=VERTEX_POINT('',#40849);
#12037=VERTEX_POINT('',#40851);
#12038=VERTEX_POINT('',#40855);
#12039=VERTEX_POINT('',#40856);
#12040=VERTEX_POINT('',#40875);
#12041=VERTEX_POINT('',#40898);
#12042=VERTEX_POINT('',#40900);
#12043=VERTEX_POINT('',#40939);
#12044=VERTEX_POINT('',#40940);
#12045=VERTEX_POINT('',#40942);
#12046=VERTEX_POINT('',#40947);
#12047=VERTEX_POINT('',#40949);
#12048=VERTEX_POINT('',#40988);
#12049=VERTEX_POINT('',#40989);
#12050=VERTEX_POINT('',#40991);
#12051=VERTEX_POINT('',#40996);
#12052=VERTEX_POINT('',#40998);
#12053=VERTEX_POINT('',#41002);
#12054=VERTEX_POINT('',#41003);
#12055=VERTEX_POINT('',#41005);
#12056=VERTEX_POINT('',#41007);
#12057=VERTEX_POINT('',#41011);
#12058=VERTEX_POINT('',#41013);
#12059=VERTEX_POINT('',#41019);
#12060=VERTEX_POINT('',#41020);
#12061=VERTEX_POINT('',#41022);
#12062=VERTEX_POINT('',#41024);
#12063=VERTEX_POINT('',#41026);
#12064=VERTEX_POINT('',#41028);
#12065=VERTEX_POINT('',#41032);
#12066=VERTEX_POINT('',#41033);
#12067=VERTEX_POINT('',#41035);
#12068=VERTEX_POINT('',#41037);
#12069=VERTEX_POINT('',#41041);
#12070=VERTEX_POINT('',#41042);
#12071=VERTEX_POINT('',#41044);
#12072=VERTEX_POINT('',#41046);
#12073=VERTEX_POINT('',#41050);
#12074=VERTEX_POINT('',#41051);
#12075=VERTEX_POINT('',#41053);
#12076=VERTEX_POINT('',#41055);
#12077=VERTEX_POINT('',#41075);
#12078=VERTEX_POINT('',#41078);
#12079=VERTEX_POINT('',#41083);
#12080=VERTEX_POINT('',#41088);
#12081=VERTEX_POINT('',#41093);
#12082=VERTEX_POINT('',#41098);
#15095=EDGE_CURVE('',#12031,#12032,#6811,.T.);
#15096=EDGE_CURVE('',#12033,#12032,#10116,.T.);
#15097=EDGE_CURVE('',#12034,#12033,#10117,.T.);
#15098=EDGE_CURVE('',#12035,#12034,#10118,.T.);
#15099=EDGE_CURVE('',#12036,#12035,#10119,.T.);
#15100=EDGE_CURVE('',#12037,#12036,#10120,.T.);
#15101=EDGE_CURVE('',#12032,#12037,#10121,.T.);
#15102=EDGE_CURVE('',#12038,#12039,#128,.T.);
#15103=EDGE_CURVE('',#12039,#12040,#6812,.T.);
#15104=EDGE_CURVE('',#12040,#12040,#10122,.T.);
#15105=EDGE_CURVE('',#12039,#12038,#129,.T.);
#15106=EDGE_CURVE('',#12040,#12041,#6813,.T.);
#15107=EDGE_CURVE('',#12041,#12042,#130,.T.);
#15108=EDGE_CURVE('',#12042,#12041,#131,.T.);
#15109=EDGE_CURVE('',#12043,#12044,#10123,.T.);
#15110=EDGE_CURVE('',#12044,#12045,#6814,.T.);
#15111=EDGE_CURVE('',#12045,#12045,#10124,.T.);
#15112=EDGE_CURVE('',#12044,#12043,#10125,.T.);
#15113=EDGE_CURVE('',#12043,#12046,#6815,.T.);
#15114=EDGE_CURVE('',#12046,#12047,#132,.T.);
#15115=EDGE_CURVE('',#12047,#12046,#133,.T.);
#15116=EDGE_CURVE('',#12048,#12049,#10126,.T.);
#15117=EDGE_CURVE('',#12049,#12050,#6816,.T.);
#15118=EDGE_CURVE('',#12050,#12050,#10127,.T.);
#15119=EDGE_CURVE('',#12049,#12048,#10128,.T.);
#15120=EDGE_CURVE('',#12051,#12051,#10129,.T.);
#15121=EDGE_CURVE('',#12051,#12052,#6817,.T.);
#15122=EDGE_CURVE('',#12052,#12052,#10130,.T.);
#15123=EDGE_CURVE('',#12053,#12054,#10131,.T.);
#15124=EDGE_CURVE('',#12054,#12055,#6818,.T.);
#15125=EDGE_CURVE('',#12056,#12055,#10132,.T.);
#15126=EDGE_CURVE('',#12056,#12053,#6819,.T.);
#15127=EDGE_CURVE('',#12057,#12057,#10133,.T.);
#15128=EDGE_CURVE('',#12057,#12058,#6820,.T.);
#15129=EDGE_CURVE('',#12058,#12058,#10134,.T.);
#15130=EDGE_CURVE('',#12048,#12051,#6821,.T.);
#15131=EDGE_CURVE('',#12059,#12060,#10135,.T.);
#15132=EDGE_CURVE('',#12060,#12061,#10136,.T.);
#15133=EDGE_CURVE('',#12061,#12062,#10137,.T.);
#15134=EDGE_CURVE('',#12062,#12063,#10138,.T.);
#15135=EDGE_CURVE('',#12063,#12064,#10139,.T.);
#15136=EDGE_CURVE('',#12064,#12059,#10140,.T.);
#15137=EDGE_CURVE('',#12065,#12066,#10141,.T.);
#15138=EDGE_CURVE('',#12066,#12067,#6822,.T.);
#15139=EDGE_CURVE('',#12068,#12067,#10142,.T.);
#15140=EDGE_CURVE('',#12068,#12065,#6823,.T.);
#15141=EDGE_CURVE('',#12069,#12070,#10143,.T.);
#15142=EDGE_CURVE('',#12070,#12071,#6824,.T.);
#15143=EDGE_CURVE('',#12072,#12071,#10144,.T.);
#15144=EDGE_CURVE('',#12072,#12069,#6825,.T.);
#15145=EDGE_CURVE('',#12073,#12074,#10145,.T.);
#15146=EDGE_CURVE('',#12074,#12075,#6826,.T.);
#15147=EDGE_CURVE('',#12076,#12075,#10146,.T.);
#15148=EDGE_CURVE('',#12076,#12073,#6827,.T.);
#15149=EDGE_CURVE('',#12071,#12056,#6828,.T.);
#15150=EDGE_CURVE('',#12055,#12068,#6829,.T.);
#15151=EDGE_CURVE('',#12067,#12076,#6830,.T.);
#15152=EDGE_CURVE('',#12075,#12072,#6831,.T.);
#15153=EDGE_CURVE('',#12053,#12070,#6832,.T.);
#15154=EDGE_CURVE('',#12069,#12074,#6833,.T.);
#15155=EDGE_CURVE('',#12073,#12066,#6834,.T.);
#15156=EDGE_CURVE('',#12065,#12054,#6835,.T.);
#15157=EDGE_CURVE('',#12077,#12060,#6836,.T.);
#15158=EDGE_CURVE('',#12037,#12077,#6837,.T.);
#15159=EDGE_CURVE('',#12078,#12037,#6838,.T.);
#15160=EDGE_CURVE('',#12078,#12061,#6839,.T.);
#15161=EDGE_CURVE('',#12036,#12078,#6840,.T.);
#15162=EDGE_CURVE('',#12079,#12036,#6841,.T.);
#15163=EDGE_CURVE('',#12079,#12062,#6842,.T.);
#15164=EDGE_CURVE('',#12035,#12079,#6843,.T.);
#15165=EDGE_CURVE('',#12080,#12035,#6844,.T.);
#15166=EDGE_CURVE('',#12080,#12063,#6845,.T.);
#15167=EDGE_CURVE('',#12034,#12080,#6846,.T.);
#15168=EDGE_CURVE('',#12081,#12034,#6847,.T.);
#15169=EDGE_CURVE('',#12081,#12064,#6848,.T.);
#15170=EDGE_CURVE('',#12033,#12081,#6849,.T.);
#15171=EDGE_CURVE('',#12082,#12033,#6850,.T.);
#15172=EDGE_CURVE('',#12082,#12059,#6851,.T.);
#15173=EDGE_CURVE('',#12032,#12082,#6852,.T.);
#15174=EDGE_CURVE('',#12077,#12032,#6853,.T.);
#20804=ORIENTED_EDGE('',*,*,#15095,.T.);
#20805=ORIENTED_EDGE('',*,*,#15096,.F.);
#20806=ORIENTED_EDGE('',*,*,#15097,.F.);
#20807=ORIENTED_EDGE('',*,*,#15098,.F.);
#20808=ORIENTED_EDGE('',*,*,#15099,.F.);
#20809=ORIENTED_EDGE('',*,*,#15100,.F.);
#20810=ORIENTED_EDGE('',*,*,#15101,.F.);
#20811=ORIENTED_EDGE('',*,*,#15095,.F.);
#20812=ORIENTED_EDGE('',*,*,#15102,.T.);
#20813=ORIENTED_EDGE('',*,*,#15103,.T.);
#20814=ORIENTED_EDGE('',*,*,#15104,.T.);
#20815=ORIENTED_EDGE('',*,*,#15103,.F.);
#20816=ORIENTED_EDGE('',*,*,#15105,.T.);
#20817=ORIENTED_EDGE('',*,*,#15104,.F.);
#20818=ORIENTED_EDGE('',*,*,#15106,.T.);
#20819=ORIENTED_EDGE('',*,*,#15107,.T.);
#20820=ORIENTED_EDGE('',*,*,#15108,.T.);
#20821=ORIENTED_EDGE('',*,*,#15106,.F.);
#20822=ORIENTED_EDGE('',*,*,#15109,.T.);
#20823=ORIENTED_EDGE('',*,*,#15110,.T.);
#20824=ORIENTED_EDGE('',*,*,#15111,.F.);
#20825=ORIENTED_EDGE('',*,*,#15110,.F.);
#20826=ORIENTED_EDGE('',*,*,#15112,.T.);
#20827=ORIENTED_EDGE('',*,*,#15109,.F.);
#20828=ORIENTED_EDGE('',*,*,#15113,.T.);
#20829=ORIENTED_EDGE('',*,*,#15114,.T.);
#20830=ORIENTED_EDGE('',*,*,#15115,.T.);
#20831=ORIENTED_EDGE('',*,*,#15113,.F.);
#20832=ORIENTED_EDGE('',*,*,#15112,.F.);
#20833=ORIENTED_EDGE('',*,*,#15116,.T.);
#20834=ORIENTED_EDGE('',*,*,#15117,.T.);
#20835=ORIENTED_EDGE('',*,*,#15118,.F.);
#20836=ORIENTED_EDGE('',*,*,#15117,.F.);
#20837=ORIENTED_EDGE('',*,*,#15119,.T.);
#20838=ORIENTED_EDGE('',*,*,#15120,.F.);
#20839=ORIENTED_EDGE('',*,*,#15121,.T.);
#20840=ORIENTED_EDGE('',*,*,#15122,.T.);
#20841=ORIENTED_EDGE('',*,*,#15121,.F.);
#20842=ORIENTED_EDGE('',*,*,#15123,.T.);
#20843=ORIENTED_EDGE('',*,*,#15124,.T.);
#20844=ORIENTED_EDGE('',*,*,#15125,.F.);
#20845=ORIENTED_EDGE('',*,*,#15126,.T.);
#20846=ORIENTED_EDGE('',*,*,#15127,.F.);
#20847=ORIENTED_EDGE('',*,*,#15128,.T.);
#20848=ORIENTED_EDGE('',*,*,#15129,.T.);
#20849=ORIENTED_EDGE('',*,*,#15128,.F.);
#20850=ORIENTED_EDGE('',*,*,#15116,.F.);
#20851=ORIENTED_EDGE('',*,*,#15130,.T.);
#20852=ORIENTED_EDGE('',*,*,#15120,.T.);
#20853=ORIENTED_EDGE('',*,*,#15130,.F.);
#20854=ORIENTED_EDGE('',*,*,#15119,.F.);
#20855=ORIENTED_EDGE('',*,*,#15115,.F.);
#20856=ORIENTED_EDGE('',*,*,#15114,.F.);
#20857=ORIENTED_EDGE('',*,*,#15108,.F.);
#20858=ORIENTED_EDGE('',*,*,#15107,.F.);
#20859=ORIENTED_EDGE('',*,*,#15131,.T.);
#20860=ORIENTED_EDGE('',*,*,#15132,.T.);
#20861=ORIENTED_EDGE('',*,*,#15133,.T.);
#20862=ORIENTED_EDGE('',*,*,#15134,.T.);
#20863=ORIENTED_EDGE('',*,*,#15135,.T.);
#20864=ORIENTED_EDGE('',*,*,#15136,.T.);
#20865=ORIENTED_EDGE('',*,*,#15137,.T.);
#20866=ORIENTED_EDGE('',*,*,#15138,.T.);
#20867=ORIENTED_EDGE('',*,*,#15139,.F.);
#20868=ORIENTED_EDGE('',*,*,#15140,.T.);
#20869=ORIENTED_EDGE('',*,*,#15102,.F.);
#20870=ORIENTED_EDGE('',*,*,#15105,.F.);
#20871=ORIENTED_EDGE('',*,*,#15141,.T.);
#20872=ORIENTED_EDGE('',*,*,#15142,.T.);
#20873=ORIENTED_EDGE('',*,*,#15143,.F.);
#20874=ORIENTED_EDGE('',*,*,#15144,.T.);
#20875=ORIENTED_EDGE('',*,*,#15145,.T.);
#20876=ORIENTED_EDGE('',*,*,#15146,.T.);
#20877=ORIENTED_EDGE('',*,*,#15147,.F.);
#20878=ORIENTED_EDGE('',*,*,#15148,.T.);
#20879=ORIENTED_EDGE('',*,*,#15127,.T.);
#20880=ORIENTED_EDGE('',*,*,#15122,.F.);
#20881=ORIENTED_EDGE('',*,*,#15143,.T.);
#20882=ORIENTED_EDGE('',*,*,#15149,.T.);
#20883=ORIENTED_EDGE('',*,*,#15125,.T.);
#20884=ORIENTED_EDGE('',*,*,#15150,.T.);
#20885=ORIENTED_EDGE('',*,*,#15139,.T.);
#20886=ORIENTED_EDGE('',*,*,#15151,.T.);
#20887=ORIENTED_EDGE('',*,*,#15147,.T.);
#20888=ORIENTED_EDGE('',*,*,#15152,.T.);
#20889=ORIENTED_EDGE('',*,*,#15129,.F.);
#20890=ORIENTED_EDGE('',*,*,#15123,.F.);
#20891=ORIENTED_EDGE('',*,*,#15153,.T.);
#20892=ORIENTED_EDGE('',*,*,#15141,.F.);
#20893=ORIENTED_EDGE('',*,*,#15154,.T.);
#20894=ORIENTED_EDGE('',*,*,#15145,.F.);
#20895=ORIENTED_EDGE('',*,*,#15155,.T.);
#20896=ORIENTED_EDGE('',*,*,#15137,.F.);
#20897=ORIENTED_EDGE('',*,*,#15156,.T.);
#20898=ORIENTED_EDGE('',*,*,#15118,.T.);
#20899=ORIENTED_EDGE('',*,*,#15156,.F.);
#20900=ORIENTED_EDGE('',*,*,#15140,.F.);
#20901=ORIENTED_EDGE('',*,*,#15150,.F.);
#20902=ORIENTED_EDGE('',*,*,#15124,.F.);
#20903=ORIENTED_EDGE('',*,*,#15155,.F.);
#20904=ORIENTED_EDGE('',*,*,#15148,.F.);
#20905=ORIENTED_EDGE('',*,*,#15151,.F.);
#20906=ORIENTED_EDGE('',*,*,#15138,.F.);
#20907=ORIENTED_EDGE('',*,*,#15154,.F.);
#20908=ORIENTED_EDGE('',*,*,#15144,.F.);
#20909=ORIENTED_EDGE('',*,*,#15152,.F.);
#20910=ORIENTED_EDGE('',*,*,#15146,.F.);
#20911=ORIENTED_EDGE('',*,*,#15153,.F.);
#20912=ORIENTED_EDGE('',*,*,#15126,.F.);
#20913=ORIENTED_EDGE('',*,*,#15149,.F.);
#20914=ORIENTED_EDGE('',*,*,#15142,.F.);
#20915=ORIENTED_EDGE('',*,*,#15111,.T.);
#20916=ORIENTED_EDGE('',*,*,#15157,.F.);
#20917=ORIENTED_EDGE('',*,*,#15158,.F.);
#20918=ORIENTED_EDGE('',*,*,#15159,.F.);
#20919=ORIENTED_EDGE('',*,*,#15160,.T.);
#20920=ORIENTED_EDGE('',*,*,#15132,.F.);
#20921=ORIENTED_EDGE('',*,*,#15160,.F.);
#20922=ORIENTED_EDGE('',*,*,#15161,.F.);
#20923=ORIENTED_EDGE('',*,*,#15162,.F.);
#20924=ORIENTED_EDGE('',*,*,#15163,.T.);
#20925=ORIENTED_EDGE('',*,*,#15133,.F.);
#20926=ORIENTED_EDGE('',*,*,#15163,.F.);
#20927=ORIENTED_EDGE('',*,*,#15164,.F.);
#20928=ORIENTED_EDGE('',*,*,#15165,.F.);
#20929=ORIENTED_EDGE('',*,*,#15166,.T.);
#20930=ORIENTED_EDGE('',*,*,#15134,.F.);
#20931=ORIENTED_EDGE('',*,*,#15166,.F.);
#20932=ORIENTED_EDGE('',*,*,#15167,.F.);
#20933=ORIENTED_EDGE('',*,*,#15168,.F.);
#20934=ORIENTED_EDGE('',*,*,#15169,.T.);
#20935=ORIENTED_EDGE('',*,*,#15135,.F.);
#20936=ORIENTED_EDGE('',*,*,#15169,.F.);
#20937=ORIENTED_EDGE('',*,*,#15170,.F.);
#20938=ORIENTED_EDGE('',*,*,#15171,.F.);
#20939=ORIENTED_EDGE('',*,*,#15172,.T.);
#20940=ORIENTED_EDGE('',*,*,#15136,.F.);
#20941=ORIENTED_EDGE('',*,*,#15172,.F.);
#20942=ORIENTED_EDGE('',*,*,#15173,.F.);
#20943=ORIENTED_EDGE('',*,*,#15174,.F.);
#20944=ORIENTED_EDGE('',*,*,#15157,.T.);
#20945=ORIENTED_EDGE('',*,*,#15131,.F.);
#20946=ORIENTED_EDGE('',*,*,#15158,.T.);
#20947=ORIENTED_EDGE('',*,*,#15174,.T.);
#20948=ORIENTED_EDGE('',*,*,#15101,.T.);
#20949=ORIENTED_EDGE('',*,*,#15173,.T.);
#20950=ORIENTED_EDGE('',*,*,#15171,.T.);
#20951=ORIENTED_EDGE('',*,*,#15096,.T.);
#20952=ORIENTED_EDGE('',*,*,#15170,.T.);
#20953=ORIENTED_EDGE('',*,*,#15168,.T.);
#20954=ORIENTED_EDGE('',*,*,#15097,.T.);
#20955=ORIENTED_EDGE('',*,*,#15167,.T.);
#20956=ORIENTED_EDGE('',*,*,#15165,.T.);
#20957=ORIENTED_EDGE('',*,*,#15098,.T.);
#20958=ORIENTED_EDGE('',*,*,#15164,.T.);
#20959=ORIENTED_EDGE('',*,*,#15162,.T.);
#20960=ORIENTED_EDGE('',*,*,#15099,.T.);
#20961=ORIENTED_EDGE('',*,*,#15161,.T.);
#20962=ORIENTED_EDGE('',*,*,#15159,.T.);
#20963=ORIENTED_EDGE('',*,*,#15100,.T.);
#24078=CYLINDRICAL_SURFACE('',#27610,2.);
#24079=CYLINDRICAL_SURFACE('',#27617,2.);
#24080=CYLINDRICAL_SURFACE('',#27625,12.5);
#24081=CYLINDRICAL_SURFACE('',#27628,10.5);
#24082=CYLINDRICAL_SURFACE('',#27631,6.9585);
#24083=CYLINDRICAL_SURFACE('',#27632,12.5);
#24084=CYLINDRICAL_SURFACE('',#27639,12.5);
#24085=CYLINDRICAL_SURFACE('',#27642,12.5);
#24086=CYLINDRICAL_SURFACE('',#27645,12.5);
#25017=ADVANCED_FACE('',(#3064),#546,.F.);
#25018=ADVANCED_FACE('',(#3065),#24078,.F.);
#25019=ADVANCED_FACE('',(#3066),#547,.T.);
#25020=ADVANCED_FACE('',(#3067),#548,.T.);
#25021=ADVANCED_FACE('',(#3068),#24079,.F.);
#25022=ADVANCED_FACE('',(#3069),#549,.F.);
#25023=ADVANCED_FACE('',(#3070),#550,.F.);
#25024=ADVANCED_FACE('',(#3071),#24080,.T.);
#25025=ADVANCED_FACE('',(#3072),#24081,.T.);
#25026=ADVANCED_FACE('',(#3073,#1373),#24082,.F.);
#25027=ADVANCED_FACE('',(#3074,#1374),#24083,.T.);
#25028=ADVANCED_FACE('',(#3075,#1375),#24084,.T.);
#25029=ADVANCED_FACE('',(#3076),#24085,.T.);
#25030=ADVANCED_FACE('',(#3077),#24086,.T.);
#25031=ADVANCED_FACE('',(#3078,#1376),#1982,.F.);
#25032=ADVANCED_FACE('',(#3079,#1377),#1983,.F.);
#25033=ADVANCED_FACE('',(#3080,#1378),#1984,.F.);
#25034=ADVANCED_FACE('',(#3081),#1985,.F.);
#25035=ADVANCED_FACE('',(#3082),#1986,.F.);
#25036=ADVANCED_FACE('',(#3083),#1987,.F.);
#25037=ADVANCED_FACE('',(#3084),#1988,.F.);
#25038=ADVANCED_FACE('',(#3085),#1989,.T.);
#25039=ADVANCED_FACE('',(#3086),#1990,.F.);
#25040=ADVANCED_FACE('',(#3087),#1991,.F.);
#25041=ADVANCED_FACE('',(#3088),#1992,.F.);
#25042=ADVANCED_FACE('',(#3089),#1993,.F.);
#25043=ADVANCED_FACE('',(#3090),#1994,.F.);
#25044=ADVANCED_FACE('',(#3091),#1995,.F.);
#25045=ADVANCED_FACE('',(#3092),#1996,.T.);
#25046=ADVANCED_FACE('',(#3093),#1997,.T.);
#25047=ADVANCED_FACE('',(#3094),#1998,.T.);
#25048=ADVANCED_FACE('',(#3095),#1999,.T.);
#25049=ADVANCED_FACE('',(#3096),#2000,.T.);
#25050=ADVANCED_FACE('',(#3097),#2001,.T.);
#25678=CLOSED_SHELL('',(#25017,#25018,#25019,#25020,#25021,#25022,#25023,
#25024,#25025,#25026,#25027,#25028,#25029,#25030,#25031,#25032,#25033,#25034,
#25035,#25036,#25037,#25038,#25039,#25040,#25041,#25042,#25043,#25044,#25045,
#25046,#25047,#25048,#25049,#25050));
#27602=AXIS2_PLACEMENT_3D('',#40838,#33206,#33207);
#27603=AXIS2_PLACEMENT_3D('',#40839,#33208,#33209);
#27604=AXIS2_PLACEMENT_3D('',#40844,#33211,#33212);
#27605=AXIS2_PLACEMENT_3D('',#40846,#33213,#33214);
#27606=AXIS2_PLACEMENT_3D('',#40848,#33215,#33216);
#27607=AXIS2_PLACEMENT_3D('',#40850,#33217,#33218);
#27608=AXIS2_PLACEMENT_3D('',#40852,#33219,#33220);
#27609=AXIS2_PLACEMENT_3D('',#40853,#33221,#33222);
#27610=AXIS2_PLACEMENT_3D('',#40854,#33223,#33224);
#27611=AXIS2_PLACEMENT_3D('',#40877,#33226,#33227);
#27612=AXIS2_PLACEMENT_3D('',#40897,#33228,#33229);
#27613=AXIS2_PLACEMENT_3D('',#40938,#33231,#33232);
#27614=AXIS2_PLACEMENT_3D('',#40941,#33233,#33234);
#27615=AXIS2_PLACEMENT_3D('',#40944,#33236,#33237);
#27616=AXIS2_PLACEMENT_3D('',#40945,#33238,#33239);
#27617=AXIS2_PLACEMENT_3D('',#40946,#33240,#33241);
#27618=AXIS2_PLACEMENT_3D('',#40987,#33243,#33244);
#27619=AXIS2_PLACEMENT_3D('',#40990,#33245,#33246);
#27620=AXIS2_PLACEMENT_3D('',#40993,#33248,#33249);
#27621=AXIS2_PLACEMENT_3D('',#40994,#33250,#33251);
#27622=AXIS2_PLACEMENT_3D('',#40995,#33252,#33253);
#27623=AXIS2_PLACEMENT_3D('',#40997,#33254,#33255);
#27624=AXIS2_PLACEMENT_3D('',#41000,#33257,#33258);
#27625=AXIS2_PLACEMENT_3D('',#41001,#33259,#33260);
#27626=AXIS2_PLACEMENT_3D('',#41004,#33261,#33262);
#27627=AXIS2_PLACEMENT_3D('',#41008,#33264,#33265);
#27628=AXIS2_PLACEMENT_3D('',#41010,#33267,#33268);
#27629=AXIS2_PLACEMENT_3D('',#41012,#33269,#33270);
#27630=AXIS2_PLACEMENT_3D('',#41015,#33272,#33273);
#27631=AXIS2_PLACEMENT_3D('',#41016,#33274,#33275);
#27632=AXIS2_PLACEMENT_3D('',#41018,#33277,#33278);
#27633=AXIS2_PLACEMENT_3D('',#41021,#33279,#33280);
#27634=AXIS2_PLACEMENT_3D('',#41023,#33281,#33282);
#27635=AXIS2_PLACEMENT_3D('',#41025,#33283,#33284);
#27636=AXIS2_PLACEMENT_3D('',#41027,#33285,#33286);
#27637=AXIS2_PLACEMENT_3D('',#41029,#33287,#33288);
#27638=AXIS2_PLACEMENT_3D('',#41030,#33289,#33290);
#27639=AXIS2_PLACEMENT_3D('',#41031,#33291,#33292);
#27640=AXIS2_PLACEMENT_3D('',#41034,#33293,#33294);
#27641=AXIS2_PLACEMENT_3D('',#41038,#33296,#33297);
#27642=AXIS2_PLACEMENT_3D('',#41040,#33299,#33300);
#27643=AXIS2_PLACEMENT_3D('',#41043,#33301,#33302);
#27644=AXIS2_PLACEMENT_3D('',#41047,#33304,#33305);
#27645=AXIS2_PLACEMENT_3D('',#41049,#33307,#33308);
#27646=AXIS2_PLACEMENT_3D('',#41052,#33309,#33310);
#27647=AXIS2_PLACEMENT_3D('',#41056,#33312,#33313);
#27648=AXIS2_PLACEMENT_3D('',#41058,#33315,#33316);
#27649=AXIS2_PLACEMENT_3D('',#41059,#33317,#33318);
#27650=AXIS2_PLACEMENT_3D('',#41064,#33323,#33324);
#27651=AXIS2_PLACEMENT_3D('',#41069,#33329,#33330);
#27652=AXIS2_PLACEMENT_3D('',#41070,#33331,#33332);
#27653=AXIS2_PLACEMENT_3D('',#41071,#33333,#33334);
#27654=AXIS2_PLACEMENT_3D('',#41072,#33335,#33336);
#27655=AXIS2_PLACEMENT_3D('',#41073,#33337,#33338);
#27656=AXIS2_PLACEMENT_3D('',#41074,#33339,#33340);
#27657=AXIS2_PLACEMENT_3D('',#41081,#33345,#33346);
#27658=AXIS2_PLACEMENT_3D('',#41086,#33350,#33351);
#27659=AXIS2_PLACEMENT_3D('',#41091,#33355,#33356);
#27660=AXIS2_PLACEMENT_3D('',#41096,#33360,#33361);
#27661=AXIS2_PLACEMENT_3D('',#41101,#33365,#33366);
#27662=AXIS2_PLACEMENT_3D('',#41104,#33369,#33370);
#27663=AXIS2_PLACEMENT_3D('',#41105,#33371,#33372);
#27664=AXIS2_PLACEMENT_3D('',#41106,#33373,#33374);
#27665=AXIS2_PLACEMENT_3D('',#41107,#33375,#33376);
#27666=AXIS2_PLACEMENT_3D('',#41108,#33377,#33378);
#27667=AXIS2_PLACEMENT_3D('',#41109,#33379,#33380);
#33206=DIRECTION('axis',(0.,0.,1.));
#33207=DIRECTION('refdir',(1.,0.,0.));
#33208=DIRECTION('center_axis',(-2.66880534765663E-16,1.,0.));
#33209=DIRECTION('ref_axis',(-1.,-2.66880534765663E-16,0.));
#33210=DIRECTION('',(0.85716730070211,0.515038074910058,-1.04972719113862E-16));
#33211=DIRECTION('center_axis',(2.66880534765663E-16,-1.,0.));
#33212=DIRECTION('ref_axis',(1.,2.66880534765663E-16,0.));
#33213=DIRECTION('center_axis',(2.66880534765663E-16,-1.,0.));
#33214=DIRECTION('ref_axis',(1.,2.66880534765663E-16,0.));
#33215=DIRECTION('center_axis',(2.66880534765663E-16,-1.,0.));
#33216=DIRECTION('ref_axis',(1.,2.66880534765663E-16,0.));
#33217=DIRECTION('center_axis',(2.66880534765663E-16,-1.,0.));
#33218=DIRECTION('ref_axis',(1.,2.66880534765663E-16,0.));
#33219=DIRECTION('center_axis',(2.66880534765663E-16,-1.,0.));
#33220=DIRECTION('ref_axis',(1.,2.66880534765663E-16,0.));
#33221=DIRECTION('center_axis',(2.66880534765663E-16,-1.,0.));
#33222=DIRECTION('ref_axis',(1.,2.66880534765663E-16,0.));
#33223=DIRECTION('center_axis',(2.66880534765663E-16,-1.,0.));
#33224=DIRECTION('ref_axis',(1.,2.66880534765663E-16,0.));
#33225=DIRECTION('',(2.66880534765663E-16,-1.,0.));
#33226=DIRECTION('center_axis',(2.66880534765663E-16,-1.,0.));
#33227=DIRECTION('ref_axis',(1.,2.66880534765663E-16,0.));
#33228=DIRECTION('center_axis',(2.66880534765663E-16,-1.,0.));
#33229=DIRECTION('ref_axis',(1.,2.66880534765663E-16,0.));
#33230=DIRECTION('',(0.707106781186543,0.707106781186552,8.65956056235488E-17));
#33231=DIRECTION('center_axis',(-2.66880534765663E-16,1.,0.));
#33232=DIRECTION('ref_axis',(-1.,-2.66880534765663E-16,0.));
#33233=DIRECTION('center_axis',(2.66880534765663E-16,-1.,0.));
#33234=DIRECTION('ref_axis',(1.,2.66880534765663E-16,0.));
#33235=DIRECTION('',(-0.707106781186542,-0.707106781186553,8.65956056235487E-17));
#33236=DIRECTION('center_axis',(2.66880534765663E-16,-1.,0.));
#33237=DIRECTION('ref_axis',(1.,2.66880534765663E-16,0.));
#33238=DIRECTION('center_axis',(2.66880534765663E-16,-1.,0.));
#33239=DIRECTION('ref_axis',(1.,2.66880534765663E-16,0.));
#33240=DIRECTION('center_axis',(2.66880534765663E-16,-1.,0.));
#33241=DIRECTION('ref_axis',(1.,2.66880534765663E-16,0.));
#33242=DIRECTION('',(2.66880534765663E-16,-1.,0.));
#33243=DIRECTION('center_axis',(1.,0.,0.));
#33244=DIRECTION('ref_axis',(0.,0.,-1.));
#33245=DIRECTION('center_axis',(-1.,0.,0.));
#33246=DIRECTION('ref_axis',(0.,0.,1.));
#33247=DIRECTION('',(0.707106781186546,-8.65956056235495E-17,0.707106781186549));
#33248=DIRECTION('center_axis',(-1.,0.,0.));
#33249=DIRECTION('ref_axis',(0.,0.,1.));
#33250=DIRECTION('center_axis',(-1.,0.,0.));
#33251=DIRECTION('ref_axis',(0.,0.,1.));
#33252=DIRECTION('center_axis',(-1.,0.,0.));
#33253=DIRECTION('ref_axis',(0.,0.,1.));
#33254=DIRECTION('center_axis',(-1.,0.,0.));
#33255=DIRECTION('ref_axis',(0.,0.,1.));
#33256=DIRECTION('',(-0.707106781186548,-8.65956056235493E-17,-0.707106781186547));
#33257=DIRECTION('center_axis',(-1.,0.,0.));
#33258=DIRECTION('ref_axis',(0.,0.,1.));
#33259=DIRECTION('center_axis',(-1.,0.,0.));
#33260=DIRECTION('ref_axis',(0.,0.,1.));
#33261=DIRECTION('center_axis',(-1.,0.,0.));
#33262=DIRECTION('ref_axis',(0.,0.,1.));
#33263=DIRECTION('',(-1.,0.,0.));
#33264=DIRECTION('center_axis',(-1.,0.,0.));
#33265=DIRECTION('ref_axis',(0.,0.,1.));
#33266=DIRECTION('',(1.,0.,0.));
#33267=DIRECTION('center_axis',(-1.,0.,0.));
#33268=DIRECTION('ref_axis',(0.,0.,1.));
#33269=DIRECTION('center_axis',(-1.,0.,0.));
#33270=DIRECTION('ref_axis',(0.,0.,1.));
#33271=DIRECTION('',(1.,0.,0.));
#33272=DIRECTION('center_axis',(-1.,0.,0.));
#33273=DIRECTION('ref_axis',(0.,0.,1.));
#33274=DIRECTION('center_axis',(-1.,0.,0.));
#33275=DIRECTION('ref_axis',(0.,0.,1.));
#33276=DIRECTION('',(-1.,0.,0.));
#33277=DIRECTION('center_axis',(-1.,0.,0.));
#33278=DIRECTION('ref_axis',(0.,0.,1.));
#33279=DIRECTION('center_axis',(1.,0.,-1.50231459873716E-15));
#33280=DIRECTION('ref_axis',(-1.50231459873716E-15,0.,-1.));
#33281=DIRECTION('center_axis',(0.500000000000006,-1.56587054853355E-13,
0.866025403784435));
#33282=DIRECTION('ref_axis',(-0.0401154877944071,0.998926588987072,0.0231606876769527));
#33283=DIRECTION('center_axis',(-0.500000000000001,-6.71087377942918E-14,
0.866025403784438));
#33284=DIRECTION('ref_axis',(0.0200049178614522,0.999733166574198,0.0115498447125027));
#33285=DIRECTION('center_axis',(-1.,0.,7.51157299368581E-16));
#33286=DIRECTION('ref_axis',(7.51157299368581E-16,0.,1.));
#33287=DIRECTION('center_axis',(-0.500000000000002,-5.59239481618774E-14,
-0.866025403784438));
#33288=DIRECTION('ref_axis',(0.0401154877945203,0.99892658898707,-0.0231606876768818));
#33289=DIRECTION('center_axis',(0.499999999999995,1.4540226522103E-13,-0.866025403784442));
#33290=DIRECTION('ref_axis',(-0.0200049178616206,0.999733166574197,-0.0115498447123624));
#33291=DIRECTION('center_axis',(-1.,0.,0.));
#33292=DIRECTION('ref_axis',(0.,0.,1.));
#33293=DIRECTION('center_axis',(-1.,0.,0.));
#33294=DIRECTION('ref_axis',(0.,0.,1.));
#33295=DIRECTION('',(-1.,0.,0.));
#33296=DIRECTION('center_axis',(-1.,0.,0.));
#33297=DIRECTION('ref_axis',(0.,0.,1.));
#33298=DIRECTION('',(1.,0.,0.));
#33299=DIRECTION('center_axis',(-1.,0.,0.));
#33300=DIRECTION('ref_axis',(0.,0.,1.));
#33301=DIRECTION('center_axis',(-1.,0.,0.));
#33302=DIRECTION('ref_axis',(0.,0.,1.));
#33303=DIRECTION('',(-1.,0.,0.));
#33304=DIRECTION('center_axis',(-1.,0.,0.));
#33305=DIRECTION('ref_axis',(0.,0.,1.));
#33306=DIRECTION('',(1.,0.,0.));
#33307=DIRECTION('center_axis',(-1.,0.,0.));
#33308=DIRECTION('ref_axis',(0.,-3.21624529935327E-16,-1.));
#33309=DIRECTION('center_axis',(-1.,0.,0.));
#33310=DIRECTION('ref_axis',(0.,0.,1.));
#33311=DIRECTION('',(-1.,0.,0.));
#33312=DIRECTION('center_axis',(-1.,0.,0.));
#33313=DIRECTION('ref_axis',(0.,0.,1.));
#33314=DIRECTION('',(1.,0.,0.));
#33315=DIRECTION('center_axis',(1.,0.,0.));
#33316=DIRECTION('ref_axis',(0.,0.,-1.));
#33317=DIRECTION('center_axis',(1.,0.,0.));
#33318=DIRECTION('ref_axis',(0.,0.,-1.));
#33319=DIRECTION('',(0.,0.707106781186548,0.707106781186547));
#33320=DIRECTION('',(0.,0.707106781186547,-0.707106781186547));
#33321=DIRECTION('',(0.,-0.707106781186547,-0.707106781186548));
#33322=DIRECTION('',(0.,-0.707106781186548,0.707106781186547));
#33323=DIRECTION('center_axis',(-1.,0.,0.));
#33324=DIRECTION('ref_axis',(0.,0.,1.));
#33325=DIRECTION('',(0.,-0.707106781186548,-0.707106781186547));
#33326=DIRECTION('',(0.,0.707106781186548,-0.707106781186547));
#33327=DIRECTION('',(0.,0.707106781186547,0.707106781186548));
#33328=DIRECTION('',(0.,-0.707106781186547,0.707106781186547));
#33329=DIRECTION('center_axis',(0.,-0.707106781186548,-0.707106781186548));
#33330=DIRECTION('ref_axis',(0.,0.707106781186548,-0.707106781186548));
#33331=DIRECTION('center_axis',(0.,-0.707106781186548,0.707106781186547));
#33332=DIRECTION('ref_axis',(0.,-0.707106781186547,-0.707106781186548));
#33333=DIRECTION('center_axis',(0.,0.707106781186547,0.707106781186548));
#33334=DIRECTION('ref_axis',(0.,-0.707106781186548,0.707106781186547));
#33335=DIRECTION('center_axis',(0.,0.707106781186547,-0.707106781186548));
#33336=DIRECTION('ref_axis',(0.,0.707106781186548,0.707106781186547));
#33337=DIRECTION('center_axis',(2.66880534765663E-16,-1.,0.));
#33338=DIRECTION('ref_axis',(1.,2.66880534765663E-16,0.));
#33339=DIRECTION('center_axis',(0.500000000000001,0.,0.866025403784438));
#33340=DIRECTION('ref_axis',(0.866025403784438,0.,-0.500000000000001));
#33341=DIRECTION('',(0.,1.,0.));
#33342=DIRECTION('',(0.866025403784438,0.,-0.500000000000001));
#33343=DIRECTION('',(0.866025403784438,0.,-0.500000000000001));
#33344=DIRECTION('',(0.,1.,0.));
#33345=DIRECTION('center_axis',(-0.499999999999999,0.,0.866025403784439));
#33346=DIRECTION('ref_axis',(0.866025403784439,0.,0.499999999999999));
#33347=DIRECTION('',(0.866025403784439,0.,0.499999999999999));
#33348=DIRECTION('',(0.866025403784439,0.,0.499999999999999));
#33349=DIRECTION('',(0.,1.,0.));
#33350=DIRECTION('center_axis',(-1.,0.,7.51157299368581E-16));
#33351=DIRECTION('ref_axis',(7.51157299368581E-16,0.,1.));
#33352=DIRECTION('',(7.51157299368581E-16,0.,1.));
#33353=DIRECTION('',(7.51157299368581E-16,0.,1.));
#33354=DIRECTION('',(0.,1.,0.));
#33355=DIRECTION('center_axis',(-0.500000000000001,0.,-0.866025403784438));
#33356=DIRECTION('ref_axis',(-0.866025403784438,0.,0.500000000000001));
#33357=DIRECTION('',(-0.866025403784438,0.,0.500000000000001));
#33358=DIRECTION('',(-0.866025403784438,0.,0.500000000000001));
#33359=DIRECTION('',(0.,1.,0.));
#33360=DIRECTION('center_axis',(0.499999999999999,0.,-0.866025403784439));
#33361=DIRECTION('ref_axis',(-0.866025403784439,0.,-0.499999999999999));
#33362=DIRECTION('',(-0.866025403784439,0.,-0.499999999999999));
#33363=DIRECTION('',(-0.866025403784439,0.,-0.499999999999999));
#33364=DIRECTION('',(0.,1.,0.));
#33365=DIRECTION('center_axis',(1.,0.,-1.50231459873716E-15));
#33366=DIRECTION('ref_axis',(-1.50231459873716E-15,0.,-1.));
#33367=DIRECTION('',(-1.50231459873716E-15,0.,-1.));
#33368=DIRECTION('',(-1.50231459873716E-15,0.,-1.));
#33369=DIRECTION('center_axis',(0.,1.,0.));
#33370=DIRECTION('ref_axis',(0.,0.,1.));
#33371=DIRECTION('center_axis',(0.,1.,0.));
#33372=DIRECTION('ref_axis',(0.,0.,1.));
#33373=DIRECTION('center_axis',(0.,1.,0.));
#33374=DIRECTION('ref_axis',(0.,0.,1.));
#33375=DIRECTION('center_axis',(0.,1.,0.));
#33376=DIRECTION('ref_axis',(0.,0.,1.));
#33377=DIRECTION('center_axis',(0.,1.,0.));
#33378=DIRECTION('ref_axis',(0.,0.,1.));
#33379=DIRECTION('center_axis',(0.,1.,0.));
#33380=DIRECTION('ref_axis',(0.,0.,1.));
#40838=CARTESIAN_POINT('',(0.,0.,0.));
#40839=CARTESIAN_POINT('Origin',(4.5,11.,0.));
#40840=CARTESIAN_POINT('',(4.5,10.3991393809724,0.));
#40841=CARTESIAN_POINT('',(5.5,11.,-1.05815080048794E-15));
#40842=CARTESIAN_POINT('',(5.5,11.,-1.22464679914735E-16));
#40843=CARTESIAN_POINT('',(5.,11.,-0.866025403784437));
#40844=CARTESIAN_POINT('Origin',(4.5,11.,0.));
#40845=CARTESIAN_POINT('',(4.,11.,-0.866025403784436));
#40846=CARTESIAN_POINT('Origin',(4.5,11.,0.));
#40847=CARTESIAN_POINT('',(3.5,11.,1.1953210976178E-15));
#40848=CARTESIAN_POINT('Origin',(4.5,11.,0.));
#40849=CARTESIAN_POINT('',(4.,11.,0.866025403784437));
#40850=CARTESIAN_POINT('Origin',(4.5,11.,0.));
#40851=CARTESIAN_POINT('',(5.,11.,0.866025403784438));
#40852=CARTESIAN_POINT('Origin',(4.5,11.,0.));
#40853=CARTESIAN_POINT('Origin',(4.5,11.,0.));
#40854=CARTESIAN_POINT('Origin',(4.5,6.,0.));
#40855=CARTESIAN_POINT('',(6.5,12.5,-8.13194945164231E-17));
#40856=CARTESIAN_POINT('',(2.5,12.5,-2.44929359829471E-16));
#40857=CARTESIAN_POINT('Ctrl Pts',(6.5,12.5,-4.16333634234434E-16));
#40858=CARTESIAN_POINT('Ctrl Pts',(6.5,12.5,-0.251586765531238));
#40859=CARTESIAN_POINT('Ctrl Pts',(6.44963191709473,12.4916317792714,-0.519649901302406));
#40860=CARTESIAN_POINT('Ctrl Pts',(6.24538925206945,12.461387706165,-1.01228304743543));
#40861=CARTESIAN_POINT('Ctrl Pts',(6.09153840204183,12.4399340066366,-1.23688872270436));
#40862=CARTESIAN_POINT('Ctrl Pts',(5.73688470830492,12.3995502329995,-1.59154241644127));
#40863=CARTESIAN_POINT('Ctrl Pts',(5.51228076000427,12.3779753882153,-1.745390117426));
#40864=CARTESIAN_POINT('Ctrl Pts',(5.01965353321852,12.3474532770021,-1.94963049432274));
#40865=CARTESIAN_POINT('Ctrl Pts',(4.75159246112229,12.3389626792531,-2.));
#40866=CARTESIAN_POINT('Ctrl Pts',(4.24840753887771,12.3389626792531,-2.));
#40867=CARTESIAN_POINT('Ctrl Pts',(3.98034646678147,12.3474532770021,-1.94963049432274));
#40868=CARTESIAN_POINT('Ctrl Pts',(3.48771923999573,12.3779753882153,-1.745390117426));
#40869=CARTESIAN_POINT('Ctrl Pts',(3.26311529169508,12.3995502329995,-1.59154241644127));
#40870=CARTESIAN_POINT('Ctrl Pts',(2.90846159795817,12.4399340066366,-1.23688872270436));
#40871=CARTESIAN_POINT('Ctrl Pts',(2.75461074793055,12.461387706165,-1.01228304743543));
#40872=CARTESIAN_POINT('Ctrl Pts',(2.55036808290527,12.4916317792714,-0.519649901302405));
#40873=CARTESIAN_POINT('Ctrl Pts',(2.5,12.5,-0.251586765531237));
#40874=CARTESIAN_POINT('Ctrl Pts',(2.5,12.5,1.38777878078145E-16));
#40875=CARTESIAN_POINT('',(2.5,12.121,-2.44929359829471E-16));
#40876=CARTESIAN_POINT('',(2.5,6.,-2.44929359829471E-16));
#40877=CARTESIAN_POINT('Origin',(4.5,12.121,0.));
#40878=CARTESIAN_POINT('Ctrl Pts',(2.5,12.5,4.85722573273506E-16));
#40879=CARTESIAN_POINT('Ctrl Pts',(2.5,12.5,0.251586765531237));
#40880=CARTESIAN_POINT('Ctrl Pts',(2.55036808290527,12.4916317792714,0.519649901302406));
#40881=CARTESIAN_POINT('Ctrl Pts',(2.75461074793055,12.461387706165,1.01228304743543));
#40882=CARTESIAN_POINT('Ctrl Pts',(2.90846159795817,12.4399340066366,1.23688872270436));
#40883=CARTESIAN_POINT('Ctrl Pts',(3.26311529169508,12.3995502329995,1.59154241644127));
#40884=CARTESIAN_POINT('Ctrl Pts',(3.48771923999573,12.3779753882153,1.745390117426));
#40885=CARTESIAN_POINT('Ctrl Pts',(3.98034646678147,12.3474532770021,1.94963049432274));
#40886=CARTESIAN_POINT('Ctrl Pts',(4.24840753887771,12.3389626792531,2.));
#40887=CARTESIAN_POINT('Ctrl Pts',(4.5,12.3389626792531,2.));
#40888=CARTESIAN_POINT('Ctrl Pts',(4.75159246112229,12.3389626792531,2.));
#40889=CARTESIAN_POINT('Ctrl Pts',(5.01965353321852,12.3474532770021,1.94963049432274));
#40890=CARTESIAN_POINT('Ctrl Pts',(5.51228076000427,12.3779753882153,1.745390117426));
#40891=CARTESIAN_POINT('Ctrl Pts',(5.73688470830492,12.3995502329995,1.59154241644127));
#40892=CARTESIAN_POINT('Ctrl Pts',(6.09153840204183,12.4399340066366,1.23688872270436));
#40893=CARTESIAN_POINT('Ctrl Pts',(6.24538925206945,12.461387706165,1.01228304743543));
#40894=CARTESIAN_POINT('Ctrl Pts',(6.44963191709473,12.4916317792714,0.519649901302405));
#40895=CARTESIAN_POINT('Ctrl Pts',(6.5,12.5,0.251586765531237));
#40896=CARTESIAN_POINT('Ctrl Pts',(6.5,12.5,-4.85722573273506E-16));
#40897=CARTESIAN_POINT('Origin',(4.5,12.121,0.));
#40898=CARTESIAN_POINT('',(2.879,12.5,-1.98515246141786E-16));
#40899=CARTESIAN_POINT('',(2.5,12.121,-2.44929359829471E-16));
#40900=CARTESIAN_POINT('',(6.121,12.5,1.28142565444101E-23));
#40901=CARTESIAN_POINT('Ctrl Pts',(2.879,12.5,-2.08166817117217E-16));
#40902=CARTESIAN_POINT('Ctrl Pts',(2.879,12.5,-0.209746160767273));
#40903=CARTESIAN_POINT('Ctrl Pts',(2.91655267539617,12.4941981000077,-0.434775598398969));
#40904=CARTESIAN_POINT('Ctrl Pts',(3.07235632722532,12.4725703604218,-0.853817682393516));
#40905=CARTESIAN_POINT('Ctrl Pts',(3.19061611370051,12.4569932358364,-1.04783985285898));
#40906=CARTESIAN_POINT('Ctrl Pts',(3.47117700763803,12.4264861212993,-1.36306503279426));
#40907=CARTESIAN_POINT('Ctrl Pts',(3.65386827011239,12.4094890721184,-1.50458240783022));
#40908=CARTESIAN_POINT('Ctrl Pts',(4.06154772862311,12.3849563429367,-1.69471072657775));
#40909=CARTESIAN_POINT('Ctrl Pts',(4.28664804766627,12.377862104465,-1.74313789553504));
#40910=CARTESIAN_POINT('Ctrl Pts',(4.71335195233373,12.377862104465,-1.74313789553504));
#40911=CARTESIAN_POINT('Ctrl Pts',(4.93845227137689,12.3849563429367,-1.69471072657775));
#40912=CARTESIAN_POINT('Ctrl Pts',(5.34613172988761,12.4094890721184,-1.50458240783022));
#40913=CARTESIAN_POINT('Ctrl Pts',(5.52882299236196,12.4264861212993,-1.36306503279425));
#40914=CARTESIAN_POINT('Ctrl Pts',(5.80938388629949,12.4569932358364,-1.04783985285898));
#40915=CARTESIAN_POINT('Ctrl Pts',(5.92764367277468,12.4725703604218,-0.853817682393517));
#40916=CARTESIAN_POINT('Ctrl Pts',(6.08344732460383,12.4941981000077,-0.43477559839897));
#40917=CARTESIAN_POINT('Ctrl Pts',(6.121,12.5,-0.209746160767274));
#40918=CARTESIAN_POINT('Ctrl Pts',(6.121,12.5,-5.55111512312578E-16));
#40919=CARTESIAN_POINT('Ctrl Pts',(6.121,12.5,-3.46944695195361E-16));
#40920=CARTESIAN_POINT('Ctrl Pts',(6.121,12.5,0.209746160767274));
#40921=CARTESIAN_POINT('Ctrl Pts',(6.08344732460383,12.4941981000077,0.43477559839897));
#40922=CARTESIAN_POINT('Ctrl Pts',(5.92764367277468,12.4725703604218,0.853817682393517));
#40923=CARTESIAN_POINT('Ctrl Pts',(5.80938388629949,12.4569932358364,1.04783985285898));
#40924=CARTESIAN_POINT('Ctrl Pts',(5.52882299236196,12.4264861212993,1.36306503279426));
#40925=CARTESIAN_POINT('Ctrl Pts',(5.34613172988761,12.4094890721184,1.50458240783022));
#40926=CARTESIAN_POINT('Ctrl Pts',(4.93845227137689,12.3849563429367,1.69471072657775));
#40927=CARTESIAN_POINT('Ctrl Pts',(4.71335195233373,12.377862104465,1.74313789553504));
#40928=CARTESIAN_POINT('Ctrl Pts',(4.5,12.377862104465,1.74313789553504));
#40929=CARTESIAN_POINT('Ctrl Pts',(4.28664804766627,12.377862104465,1.74313789553504));
#40930=CARTESIAN_POINT('Ctrl Pts',(4.06154772862311,12.3849563429367,1.69471072657775));
#40931=CARTESIAN_POINT('Ctrl Pts',(3.65386827011239,12.4094890721184,1.50458240783022));
#40932=CARTESIAN_POINT('Ctrl Pts',(3.47117700763804,12.4264861212993,1.36306503279425));
#40933=CARTESIAN_POINT('Ctrl Pts',(3.19061611370051,12.4569932358364,1.04783985285898));
#40934=CARTESIAN_POINT('Ctrl Pts',(3.07235632722532,12.4725703604218,0.853817682393517));
#40935=CARTESIAN_POINT('Ctrl Pts',(2.91655267539617,12.4941981000077,0.43477559839897));
#40936=CARTESIAN_POINT('Ctrl Pts',(2.879,12.5,0.209746160767274));
#40937=CARTESIAN_POINT('Ctrl Pts',(2.879,12.5,6.93889390390723E-17));
#40938=CARTESIAN_POINT('Origin',(4.5,7.5,0.));
#40939=CARTESIAN_POINT('',(2.5,8.25000000000001,2.44929359829471E-16));
#40940=CARTESIAN_POINT('',(6.5,8.25000000000001,-2.44929359829471E-16));
#40941=CARTESIAN_POINT('Origin',(4.5,8.25000000000001,0.));
#40942=CARTESIAN_POINT('',(5.75,7.5,-1.53080849893419E-16));
#40943=CARTESIAN_POINT('',(5.75,7.5,-1.53080849893419E-16));
#40944=CARTESIAN_POINT('Origin',(4.5,7.5,0.));
#40945=CARTESIAN_POINT('Origin',(4.5,8.25000000000001,0.));
#40946=CARTESIAN_POINT('Origin',(4.5,6.,0.));
#40947=CARTESIAN_POINT('',(2.5,6.9585,-2.6124255799288E-16));
#40948=CARTESIAN_POINT('',(2.5,6.,-2.44929359829471E-16));
#40949=CARTESIAN_POINT('',(6.5,6.9585,5.51554030451387E-17));
#40950=CARTESIAN_POINT('Ctrl Pts',(2.5,6.9585,-2.77555756156289E-16));
#40951=CARTESIAN_POINT('Ctrl Pts',(2.5,6.9585,-0.252637698086405));
#40952=CARTESIAN_POINT('Ctrl Pts',(2.55078010677237,6.94337565665523,-0.521159230418503));
#40953=CARTESIAN_POINT('Ctrl Pts',(2.75533748034076,6.88874841306866,-1.01351751722741));
#40954=CARTESIAN_POINT('Ctrl Pts',(2.90903822842602,6.84996260038966,-1.23746535317221));
#40955=CARTESIAN_POINT('Ctrl Pts',(3.26257869425884,6.77657914101289,-1.59100581900503));
#40956=CARTESIAN_POINT('Ctrl Pts',(3.48650851036758,6.7370684472136,-1.74467239254521));
#40957=CARTESIAN_POINT('Ctrl Pts',(3.9788017352627,6.68076154284702,-1.94920461648384));
#40958=CARTESIAN_POINT('Ctrl Pts',(4.2472993420588,6.66488726461296,-2.));
#40959=CARTESIAN_POINT('Ctrl Pts',(4.7527006579412,6.66488726461296,-2.));
#40960=CARTESIAN_POINT('Ctrl Pts',(5.0211982647373,6.68076154284702,-1.94920461648384));
#40961=CARTESIAN_POINT('Ctrl Pts',(5.51349148963242,6.7370684472136,-1.74467239254521));
#40962=CARTESIAN_POINT('Ctrl Pts',(5.73742130574116,6.77657914101289,-1.59100581900503));
#40963=CARTESIAN_POINT('Ctrl Pts',(6.09096177157398,6.84996260038966,-1.23746535317221));
#40964=CARTESIAN_POINT('Ctrl Pts',(6.24466251965925,6.88874841306866,-1.01351751722741));
#40965=CARTESIAN_POINT('Ctrl Pts',(6.44921989322763,6.94337565665523,-0.521159230418501));
#40966=CARTESIAN_POINT('Ctrl Pts',(6.5,6.9585,-0.252637698086404));
#40967=CARTESIAN_POINT('Ctrl Pts',(6.5,6.9585,-6.93889390390723E-17));
#40968=CARTESIAN_POINT('Ctrl Pts',(6.5,6.9585,2.08166817117217E-16));
#40969=CARTESIAN_POINT('Ctrl Pts',(6.5,6.9585,0.252637698086405));
#40970=CARTESIAN_POINT('Ctrl Pts',(6.44921989322763,6.94337565665523,0.521159230418502));
#40971=CARTESIAN_POINT('Ctrl Pts',(6.24466251965925,6.88874841306866,1.01351751722741));
#40972=CARTESIAN_POINT('Ctrl Pts',(6.09096177157398,6.84996260038966,1.23746535317221));
#40973=CARTESIAN_POINT('Ctrl Pts',(5.73742130574116,6.77657914101289,1.59100581900503));
#40974=CARTESIAN_POINT('Ctrl Pts',(5.51349148963242,6.7370684472136,1.74467239254521));
#40975=CARTESIAN_POINT('Ctrl Pts',(5.0211982647373,6.68076154284702,1.94920461648384));
#40976=CARTESIAN_POINT('Ctrl Pts',(4.7527006579412,6.66488726461296,2.));
#40977=CARTESIAN_POINT('Ctrl Pts',(4.5,6.66488726461296,2.));
#40978=CARTESIAN_POINT('Ctrl Pts',(4.2472993420588,6.66488726461296,2.));
#40979=CARTESIAN_POINT('Ctrl Pts',(3.9788017352627,6.68076154284702,1.94920461648384));
#40980=CARTESIAN_POINT('Ctrl Pts',(3.48650851036758,6.7370684472136,1.74467239254521));
#40981=CARTESIAN_POINT('Ctrl Pts',(3.26257869425884,6.77657914101289,1.59100581900503));
#40982=CARTESIAN_POINT('Ctrl Pts',(2.90903822842602,6.84996260038966,1.23746535317221));
#40983=CARTESIAN_POINT('Ctrl Pts',(2.75533748034075,6.88874841306866,1.01351751722741));
#40984=CARTESIAN_POINT('Ctrl Pts',(2.55078010677237,6.94337565665523,0.521159230418502));
#40985=CARTESIAN_POINT('Ctrl Pts',(2.5,6.9585,0.252637698086404));
#40986=CARTESIAN_POINT('Ctrl Pts',(2.5,6.9585,-2.08166817117217E-16));
#40987=CARTESIAN_POINT('Origin',(7.4585,0.,0.));
#40988=CARTESIAN_POINT('',(7.4585,8.52170475186686E-16,-6.9585));
#40989=CARTESIAN_POINT('',(7.4585,-8.52170475186686E-16,6.9585));
#40990=CARTESIAN_POINT('Origin',(7.4585,0.,0.));
#40991=CARTESIAN_POINT('',(8.,-9.18485099360515E-16,7.5));
#40992=CARTESIAN_POINT('',(7.4585,-8.52170475186686E-16,6.9585));
#40993=CARTESIAN_POINT('Origin',(8.,0.,0.));
#40994=CARTESIAN_POINT('Origin',(7.4585,0.,0.));
#40995=CARTESIAN_POINT('Origin',(0.,0.,0.));
#40996=CARTESIAN_POINT('',(0.5415,-8.52170475186686E-16,-6.9585));
#40997=CARTESIAN_POINT('Origin',(0.541499999999999,0.,0.));
#40998=CARTESIAN_POINT('',(-5.77101208116537E-16,-9.18485099360515E-16,
-7.5));
#40999=CARTESIAN_POINT('',(0.,-9.18485099360515E-16,-7.5));
#41000=CARTESIAN_POINT('Origin',(0.,0.,0.));
#41001=CARTESIAN_POINT('Origin',(-0.4,0.,0.));
#41002=CARTESIAN_POINT('',(8.,-3.57996068711535,11.9763884989887));
#41003=CARTESIAN_POINT('',(8.,3.57996068711535,11.9763884989887));
#41004=CARTESIAN_POINT('Origin',(8.,0.,0.));
#41005=CARTESIAN_POINT('',(1.,3.57996068711535,11.9763884989887));
#41006=CARTESIAN_POINT('',(-0.4,3.57996068711535,11.9763884989887));
#41007=CARTESIAN_POINT('',(1.,-3.57996068711536,11.9763884989887));
#41008=CARTESIAN_POINT('Origin',(1.,0.,0.));
#41009=CARTESIAN_POINT('',(-0.4,-3.57996068711536,11.9763884989887));
#41010=CARTESIAN_POINT('Origin',(-0.4,0.,0.));
#41011=CARTESIAN_POINT('',(0.,-1.28587913910472E-15,-10.5));
#41012=CARTESIAN_POINT('Origin',(0.,0.,0.));
#41013=CARTESIAN_POINT('',(1.,-1.28587913910472E-15,-10.5));
#41014=CARTESIAN_POINT('',(-0.4,-1.28587913910472E-15,-10.5));
#41015=CARTESIAN_POINT('Origin',(1.,0.,0.));
#41016=CARTESIAN_POINT('Origin',(0.,0.,0.));
#41017=CARTESIAN_POINT('',(0.,-8.52170475186686E-16,-6.9585));
#41018=CARTESIAN_POINT('Origin',(-0.4,0.,0.));
#41019=CARTESIAN_POINT('',(5.5,12.4866595479602,-0.577350269189626));
#41020=CARTESIAN_POINT('',(5.5,12.4866595479602,0.577350269189624));
#41021=CARTESIAN_POINT('Origin',(5.5,0.,0.));
#41022=CARTESIAN_POINT('',(4.5,12.4465524008324,1.15470053837925));
#41023=CARTESIAN_POINT('Origin',(6.49474644070762,-37.2251671136432,0.00303314386277891));
#41024=CARTESIAN_POINT('',(3.5,12.4866595479602,0.577350269189625));
#41025=CARTESIAN_POINT('Origin',(2.50525355929134,-37.2251671136413,0.00303314386722944));
#41026=CARTESIAN_POINT('',(3.5,12.4866595479602,-0.577350269189624));
#41027=CARTESIAN_POINT('Origin',(3.5,0.,0.));
#41028=CARTESIAN_POINT('',(4.5,12.4465524008324,-1.15470053837925));
#41029=CARTESIAN_POINT('Origin',(2.505253559288,-37.2251671136122,-0.00303314386702086));
#41030=CARTESIAN_POINT('Origin',(6.49474644071747,-37.2251671136628,-0.00303314387395726));
#41031=CARTESIAN_POINT('Origin',(-0.4,0.,0.));
#41032=CARTESIAN_POINT('',(8.,11.9763884989887,3.57996068711535));
#41033=CARTESIAN_POINT('',(8.,11.9763884989887,-3.57996068711535));
#41034=CARTESIAN_POINT('Origin',(8.,0.,0.));
#41035=CARTESIAN_POINT('',(1.,11.9763884989887,-3.57996068711535));
#41036=CARTESIAN_POINT('',(-0.4,11.9763884989887,-3.57996068711535));
#41037=CARTESIAN_POINT('',(1.,11.9763884989887,3.57996068711535));
#41038=CARTESIAN_POINT('Origin',(1.,0.,0.));
#41039=CARTESIAN_POINT('',(-0.4,11.9763884989887,3.57996068711535));
#41040=CARTESIAN_POINT('Origin',(-0.4,0.,0.));
#41041=CARTESIAN_POINT('',(8.,-11.9763884989887,-3.57996068711537));
#41042=CARTESIAN_POINT('',(8.,-11.9763884989887,3.57996068711536));
#41043=CARTESIAN_POINT('Origin',(8.,0.,0.));
#41044=CARTESIAN_POINT('',(1.,-11.9763884989887,3.57996068711537));
#41045=CARTESIAN_POINT('',(-0.4,-11.9763884989887,3.57996068711536));
#41046=CARTESIAN_POINT('',(1.,-11.9763884989887,-3.57996068711537));
#41047=CARTESIAN_POINT('Origin',(1.,0.,0.));
#41048=CARTESIAN_POINT('',(-0.4,-11.9763884989887,-3.57996068711537));
#41049=CARTESIAN_POINT('Origin',(-0.4,0.,0.));
#41050=CARTESIAN_POINT('',(8.,3.57996068711536,-11.9763884989887));
#41051=CARTESIAN_POINT('',(8.,-3.57996068711536,-11.9763884989887));
#41052=CARTESIAN_POINT('Origin',(8.,0.,0.));
#41053=CARTESIAN_POINT('',(1.,-3.57996068711536,-11.9763884989887));
#41054=CARTESIAN_POINT('',(-0.4,-3.57996068711536,-11.9763884989887));
#41055=CARTESIAN_POINT('',(1.,3.57996068711536,-11.9763884989887));
#41056=CARTESIAN_POINT('Origin',(1.,0.,0.));
#41057=CARTESIAN_POINT('',(-0.4,3.57996068711536,-11.9763884989887));
#41058=CARTESIAN_POINT('Origin',(0.,0.,0.));
#41059=CARTESIAN_POINT('Origin',(1.,10.5,0.));
#41060=CARTESIAN_POINT('',(1.,-2.52817459305202,13.028174593052));
#41061=CARTESIAN_POINT('',(1.,13.028174593052,2.52817459305202));
#41062=CARTESIAN_POINT('',(1.,13.028174593052,-2.52817459305202));
#41063=CARTESIAN_POINT('',(1.,-2.52817459305202,-13.028174593052));
#41064=CARTESIAN_POINT('Origin',(8.,12.5,0.));
#41065=CARTESIAN_POINT('',(8.,-1.52817459305202,14.028174593052));
#41066=CARTESIAN_POINT('',(8.,-1.52817459305202,-14.028174593052));
#41067=CARTESIAN_POINT('',(8.,14.028174593052,-1.52817459305202));
#41068=CARTESIAN_POINT('',(8.,14.028174593052,1.52817459305202));
#41069=CARTESIAN_POINT('Origin',(8.,15.556349186104,0.));
#41070=CARTESIAN_POINT('Origin',(8.,-5.42101086242754E-17,-15.556349186104));
#41071=CARTESIAN_POINT('Origin',(8.,-5.42101086242754E-17,-15.556349186104));
#41072=CARTESIAN_POINT('Origin',(8.,-15.5563491861041,-3.52365706057789E-15));
#41073=CARTESIAN_POINT('Origin',(3.25,7.5,0.));
#41074=CARTESIAN_POINT('Origin',(4.5,11.,1.15470053837925));
#41075=CARTESIAN_POINT('',(5.5,11.,0.577350269189624));
#41076=CARTESIAN_POINT('',(5.5,11.,0.577350269189624));
#41077=CARTESIAN_POINT('',(4.5,11.,1.15470053837925));
#41078=CARTESIAN_POINT('',(4.5,11.,1.15470053837925));
#41079=CARTESIAN_POINT('',(4.5,11.,1.15470053837925));
#41080=CARTESIAN_POINT('',(4.5,11.,1.15470053837925));
#41081=CARTESIAN_POINT('Origin',(3.5,11.,0.577350269189625));
#41082=CARTESIAN_POINT('',(3.5,11.,0.577350269189625));
#41083=CARTESIAN_POINT('',(3.5,11.,0.577350269189625));
#41084=CARTESIAN_POINT('',(3.5,11.,0.577350269189625));
#41085=CARTESIAN_POINT('',(3.5,11.,0.577350269189625));
#41086=CARTESIAN_POINT('Origin',(3.5,11.,-0.577350269189624));
#41087=CARTESIAN_POINT('',(3.5,11.,-0.577350269189624));
#41088=CARTESIAN_POINT('',(3.5,11.,-0.577350269189624));
#41089=CARTESIAN_POINT('',(3.5,11.,-0.577350269189624));
#41090=CARTESIAN_POINT('',(3.5,11.,-0.577350269189624));
#41091=CARTESIAN_POINT('Origin',(4.5,11.,-1.15470053837925));
#41092=CARTESIAN_POINT('',(4.5,11.,-1.15470053837925));
#41093=CARTESIAN_POINT('',(4.5,11.,-1.15470053837925));
#41094=CARTESIAN_POINT('',(4.5,11.,-1.15470053837925));
#41095=CARTESIAN_POINT('',(4.5,11.,-1.15470053837925));
#41096=CARTESIAN_POINT('Origin',(5.5,11.,-0.577350269189626));
#41097=CARTESIAN_POINT('',(5.5,11.,-0.577350269189626));
#41098=CARTESIAN_POINT('',(5.5,11.,-0.577350269189626));
#41099=CARTESIAN_POINT('',(5.5,11.,-0.577350269189626));
#41100=CARTESIAN_POINT('',(5.5,11.,-0.577350269189626));
#41101=CARTESIAN_POINT('Origin',(5.5,11.,0.577350269189624));
#41102=CARTESIAN_POINT('',(5.5,11.,0.577350269189624));
#41103=CARTESIAN_POINT('',(5.5,11.,0.577350269189624));
#41104=CARTESIAN_POINT('Origin',(0.,11.,0.));
#41105=CARTESIAN_POINT('Origin',(0.,11.,0.));
#41106=CARTESIAN_POINT('Origin',(0.,11.,0.));
#41107=CARTESIAN_POINT('Origin',(0.,11.,0.));
#41108=CARTESIAN_POINT('Origin',(0.,11.,0.));
#41109=CARTESIAN_POINT('Origin',(0.,11.,0.));
#66661=UNCERTAINTY_MEASURE_WITH_UNIT(LENGTH_MEASURE(0.01),#66722,
'DISTANCE_ACCURACY_VALUE',
'Maximum model space distance between geometric entities at asserted c
onnectivities');
#66680=UNCERTAINTY_MEASURE_WITH_UNIT(LENGTH_MEASURE(0.01),#66722,
'DISTANCE_ACCURACY_VALUE',
'Maximum model space distance between geometric entities at asserted c
onnectivities');
#66702=(
GEOMETRIC_REPRESENTATION_CONTEXT(3)
GLOBAL_UNCERTAINTY_ASSIGNED_CONTEXT((#66661))
GLOBAL_UNIT_ASSIGNED_CONTEXT((#66722,#66724,#66725))
REPRESENTATION_CONTEXT('','3D')
);
#66721=(
GEOMETRIC_REPRESENTATION_CONTEXT(3)
GLOBAL_UNCERTAINTY_ASSIGNED_CONTEXT((#66680))
GLOBAL_UNIT_ASSIGNED_CONTEXT((#66722,#66724,#66725))
REPRESENTATION_CONTEXT('','3D')
);
#66722=(
LENGTH_UNIT()
NAMED_UNIT(*)
SI_UNIT(.MILLI.,.METRE.)
);
#66724=(
NAMED_UNIT(*)
PLANE_ANGLE_UNIT()
SI_UNIT($,.RADIAN.)
);
#66725=(
NAMED_UNIT(*)
SI_UNIT($,.STERADIAN.)
SOLID_ANGLE_UNIT()
);
#66747=SHAPE_DEFINITION_REPRESENTATION(#66803,#66911);
#66803=PRODUCT_DEFINITION_SHAPE('',$,#66952);
#66911=SHAPE_REPRESENTATION('',(#27602),#66702);
#66930=PRODUCT_DEFINITION_CONTEXT('part definition',#67052,'design');
#66952=PRODUCT_DEFINITION('Lock Nut','Lock Nut',#66992,#66930);
#66992=PRODUCT_DEFINITION_FORMATION('',$,#67075);
#67052=APPLICATION_CONTEXT(
'Core Data for Automotive Mechanical Design Process');
#67053=PRODUCT_CONTEXT('part definition',#67052,'mechanical');
#67075=PRODUCT('Lock Nut','Lock Nut',$,(#67053));
#67095=PRESENTATION_STYLE_ASSIGNMENT((#67097));
#67097=SURFACE_STYLE_USAGE(.BOTH.,#67099);
#67099=SURFACE_SIDE_STYLE('',(#67101));
#67101=SURFACE_STYLE_FILL_AREA(#67103);
#67103=FILL_AREA_STYLE('Opaque(202,209,238)',(#67105));
#67105=FILL_AREA_STYLE_COLOUR('Opaque(202,209,238)',#67107);
#67107=COLOUR_RGB('Opaque(202,209,238)',0.792156862745098,0.819607843137255,
0.933333333333333);
ENDSEC;
END-ISO-10303-21;
